ISO-10303-21;
HEADER;
/* Generated by software containing ST-Developer
 * from STEP Tools, Inc. (www.steptools.com) 
 */

FILE_DESCRIPTION(
/* description */ ('PAT-001'),
/* implementation_level */ '2;1');

FILE_NAME(
/* name */ 'Journal spacer (1).step',
/* time_stamp */ '2026-10-29T17:07:15-07:00',
/* author */ (''),
/* organization */ (''),
/* preprocessor_version */ 'ST-DEVELOPER v20.2',
/* originating_system */ 'Autodesk Translation Framework v15.17.0.0',
/* authorisation */ '');

FILE_SCHEMA (('AUTOMOTIVE_DESIGN { 1 0 10303 214 3 1 1 }'));
ENDSEC;

DATA;
#10=MECHANICAL_DESIGN_GEOMETRIC_PRESENTATION_REPRESENTATION('',(#375),#9622);
#325=SHAPE_REPRESENTATION_RELATIONSHIP('SRR','None',#9748,#350);
#350=ADVANCED_BREP_SHAPE_REPRESENTATION('',(#408),#9597);
#375=STYLED_ITEM('',(#9955),#408);
#408=MANIFOLD_SOLID_BREP('Body1',#5200);
#443=FACE_BOUND('',#1035,.T.);
#444=FACE_BOUND('',#1037,.T.);
#536=PLANE('',#5549);
#537=PLANE('',#5550);
#730=FACE_OUTER_BOUND('',#1032,.T.);
#731=FACE_OUTER_BOUND('',#1033,.T.);
#732=FACE_OUTER_BOUND('',#1034,.T.);
#733=FACE_OUTER_BOUND('',#1036,.T.);
#1032=EDGE_LOOP('',(#3559,#3560,#3561,#3562));
#1033=EDGE_LOOP('',(#3563,#3564,#3565,#3566));
#1034=EDGE_LOOP('',(#3567));
#1035=EDGE_LOOP('',(#3568));
#1036=EDGE_LOOP('',(#3569));
#1037=EDGE_LOOP('',(#3570));
#1405=LINE('',#7767,#1810);
#1406=LINE('',#7773,#1811);
#1810=VECTOR('',#6186,0.505);
#1811=VECTOR('',#6193,0.8);
#2222=CIRCLE('',#5544,0.505);
#2223=CIRCLE('',#5545,0.505);
#2224=CIRCLE('',#5547,0.8);
#2225=CIRCLE('',#5548,0.8);
#2434=VERTEX_POINT('',#7764);
#2435=VERTEX_POINT('',#7766);
#2436=VERTEX_POINT('',#7770);
#2437=VERTEX_POINT('',#7772);
#2883=EDGE_CURVE('',#2434,#2434,#2222,.T.);
#2884=EDGE_CURVE('',#2434,#2435,#1405,.T.);
#2885=EDGE_CURVE('',#2435,#2435,#2223,.T.);
#2886=EDGE_CURVE('',#2436,#2436,#2224,.T.);
#2887=EDGE_CURVE('',#2436,#2437,#1406,.T.);
#2888=EDGE_CURVE('',#2437,#2437,#2225,.T.);
#3559=ORIENTED_EDGE('',*,*,#2883,.F.);
#3560=ORIENTED_EDGE('',*,*,#2884,.T.);
#3561=ORIENTED_EDGE('',*,*,#2885,.T.);
#3562=ORIENTED_EDGE('',*,*,#2884,.F.);
#3563=ORIENTED_EDGE('',*,*,#2886,.F.);
#3564=ORIENTED_EDGE('',*,*,#2887,.T.);
#3565=ORIENTED_EDGE('',*,*,#2888,.T.);
#3566=ORIENTED_EDGE('',*,*,#2887,.F.);
#3567=ORIENTED_EDGE('',*,*,#2886,.T.);
#3568=ORIENTED_EDGE('',*,*,#2883,.T.);
#3569=ORIENTED_EDGE('',*,*,#2888,.F.);
#3570=ORIENTED_EDGE('',*,*,#2885,.F.);
#4834=CYLINDRICAL_SURFACE('',#5543,0.505);
#4835=CYLINDRICAL_SURFACE('',#5546,0.8);
#4917=ADVANCED_FACE('',(#730),#4834,.F.);
#4918=ADVANCED_FACE('',(#731),#4835,.T.);
#4919=ADVANCED_FACE('',(#732,#443),#536,.T.);
#4920=ADVANCED_FACE('',(#733,#444),#537,.F.);
#5200=CLOSED_SHELL('',(#4917,#4918,#4919,#4920));
#5542=AXIS2_PLACEMENT_3D('',#7762,#6180,#6181);
#5543=AXIS2_PLACEMENT_3D('',#7763,#6182,#6183);
#5544=AXIS2_PLACEMENT_3D('',#7765,#6184,#6185);
#5545=AXIS2_PLACEMENT_3D('',#7768,#6187,#6188);
#5546=AXIS2_PLACEMENT_3D('',#7769,#6189,#6190);
#5547=AXIS2_PLACEMENT_3D('',#7771,#6191,#6192);
#5548=AXIS2_PLACEMENT_3D('',#7774,#6194,#6195);
#5549=AXIS2_PLACEMENT_3D('',#7775,#6196,#6197);
#5550=AXIS2_PLACEMENT_3D('',#7776,#6198,#6199);
#6180=DIRECTION('axis',(0.,0.,1.));
#6181=DIRECTION('refdir',(1.,0.,0.));
#6182=DIRECTION('center_axis',(0.,1.,0.));
#6183=DIRECTION('ref_axis',(1.,0.,0.));
#6184=DIRECTION('center_axis',(0.,-1.,0.));
#6185=DIRECTION('ref_axis',(1.,0.,0.));
#6186=DIRECTION('',(0.,-1.,0.));
#6187=DIRECTION('center_axis',(0.,-1.,0.));
#6188=DIRECTION('ref_axis',(1.,0.,0.));
#6189=DIRECTION('center_axis',(0.,1.,0.));
#6190=DIRECTION('ref_axis',(1.,0.,0.));
#6191=DIRECTION('center_axis',(0.,1.,0.));
#6192=DIRECTION('ref_axis',(1.,0.,0.));
#6193=DIRECTION('',(0.,-1.,0.));
#6194=DIRECTION('center_axis',(0.,1.,0.));
#6195=DIRECTION('ref_axis',(1.,0.,0.));
#6196=DIRECTION('center_axis',(0.,1.,0.));
#6197=DIRECTION('ref_axis',(1.,0.,0.));
#6198=DIRECTION('center_axis',(0.,1.,0.));
#6199=DIRECTION('ref_axis',(1.,0.,0.));
#7762=CARTESIAN_POINT('',(0.,0.,0.));
#7763=CARTESIAN_POINT('Origin',(0.,30.,4.5));
#7764=CARTESIAN_POINT('',(-0.505,31.6,4.5));
#7765=CARTESIAN_POINT('Origin',(0.,31.6,4.5));
#7766=CARTESIAN_POINT('',(-0.505,30.,4.5));
#7767=CARTESIAN_POINT('',(-0.505,30.,4.5));
#7768=CARTESIAN_POINT('Origin',(0.,30.,4.5));
#7769=CARTESIAN_POINT('Origin',(0.,30.,4.5));
#7770=CARTESIAN_POINT('',(-0.8,31.6,4.5));
#7771=CARTESIAN_POINT('Origin',(0.,31.6,4.5));
#7772=CARTESIAN_POINT('',(-0.8,30.,4.5));
#7773=CARTESIAN_POINT('',(-0.8,30.,4.5));
#7774=CARTESIAN_POINT('Origin',(0.,30.,4.5));
#7775=CARTESIAN_POINT('Origin',(0.,31.6,4.5));
#7776=CARTESIAN_POINT('Origin',(0.,30.,4.5));
#9567=UNCERTAINTY_MEASURE_WITH_UNIT(LENGTH_MEASURE(0.001),#9623,
'DISTANCE_ACCURACY_VALUE',
'Maximum model space distance between geometric entities at asserted c
onnectivities');
#9592=UNCERTAINTY_MEASURE_WITH_UNIT(LENGTH_MEASURE(0.001),#9623,
'DISTANCE_ACCURACY_VALUE',
'Maximum model space distance between geometric entities at asserted c
onnectivities');
#9597=(
GEOMETRIC_REPRESENTATION_CONTEXT(3)
GLOBAL_UNCERTAINTY_ASSIGNED_CONTEXT((#9567))
GLOBAL_UNIT_ASSIGNED_CONTEXT((#9623,#9625,#9626))
REPRESENTATION_CONTEXT('','3D')
);
#9622=(
GEOMETRIC_REPRESENTATION_CONTEXT(3)
GLOBAL_UNCERTAINTY_ASSIGNED_CONTEXT((#9592))
GLOBAL_UNIT_ASSIGNED_CONTEXT((#9623,#9625,#9626))
REPRESENTATION_CONTEXT('','3D')
);
#9623=(
LENGTH_UNIT()
NAMED_UNIT(*)
SI_UNIT(.CENTI.,.METRE.)
);
#9625=(
NAMED_UNIT(*)
PLANE_ANGLE_UNIT()
SI_UNIT($,.RADIAN.)
);
#9626=(
NAMED_UNIT(*)
SI_UNIT($,.STERADIAN.)
SOLID_ANGLE_UNIT()
);
#9631=SHAPE_DEFINITION_REPRESENTATION(#9660,#9748);
#9660=PRODUCT_DEFINITION_SHAPE('',$,#9778);
#9748=SHAPE_REPRESENTATION('',(#5542),#9597);
#9773=PRODUCT_DEFINITION_CONTEXT('part definition',#9862,'design');
#9778=PRODUCT_DEFINITION('Journal spacer (1)','Journal spacer (1)',#9807,
#9773);
#9807=PRODUCT_DEFINITION_FORMATION('',$,#9868);
#9862=APPLICATION_CONTEXT(
'Core Data for Automotive Mechanical Design Process');
#9863=PRODUCT_CONTEXT('part definition',#9862,'mechanical');
#9868=PRODUCT('Journal spacer (1)','Journal spacer (1)','Journal spacer (1)',
(#9863));
#9949=COLOUR_RGB('Sky Blue',0.24,0.69,0.87);
#9950=FILL_AREA_STYLE_COLOUR('',#9949);
#9951=FILL_AREA_STYLE('',(#9950));
#9952=SURFACE_STYLE_FILL_AREA(#9951);
#9953=SURFACE_SIDE_STYLE('',(#9952));
#9954=SURFACE_STYLE_USAGE(.BOTH.,#9953);
#9955=PRESENTATION_STYLE_ASSIGNMENT((#9954));
ENDSEC;
END-ISO-10303-21;
